ISO-10303-21;
HEADER;
FILE_DESCRIPTION((''),'2;1');
FILE_NAME('Clamp_Bolt_3.step','2026-10-09T10:15:02-07:00',(''),(''),'','','');
FILE_SCHEMA (('AUTOMOTIVE_DESIGN { 1 0 10303 214 3 1 1 }'));
ENDSEC;
DATA;
#10=MECHANICAL_DESIGN_GEOMETRIC_PRESENTATION_REPRESENTATION('',(#91),#6779);
#55=TOROIDAL_SURFACE('',#4392,4.4,0.6) ;
#56=TOROIDAL_SURFACE('',#4396,3.25,0.25) ;
#71=SHAPE_REPRESENTATION_RELATIONSHIP('SRR','None',#6825,#81) ;
#81=ADVANCED_BREP_SHAPE_REPRESENTATION('',(#101),#6777) ;
#91=STYLED_ITEM('',(#6877),#101) ;
#101=MANIFOLD_SOLID_BREP('Body1',#3903) ;
#131=FACE_BOUND('',#821,.T.) ;
#132=FACE_BOUND('',#823,.T.) ;
#243=PLANE('',#4378) ;
#244=PLANE('',#4379) ;
#245=PLANE('',#4380) ;
#246=PLANE('',#4381) ;
#247=PLANE('',#4382) ;
#248=PLANE('',#4383) ;
#249=PLANE('',#4384) ;
#250=PLANE('',#4385) ;
#251=PLANE('',#4387) ;
#252=PLANE('',#4390) ;
#325=CONICAL_SURFACE('',#4401,2.5,0.785398163397) ;
#541=FACE_OUTER_BOUND('',#813,.T.) ;
#542=FACE_OUTER_BOUND('',#814,.T.) ;
#543=FACE_OUTER_BOUND('',#815,.T.) ;
#544=FACE_OUTER_BOUND('',#816,.T.) ;
#545=FACE_OUTER_BOUND('',#817,.T.) ;
#546=FACE_OUTER_BOUND('',#818,.T.) ;
#547=FACE_OUTER_BOUND('',#819,.T.) ;
#548=FACE_OUTER_BOUND('',#820,.T.) ;
#549=FACE_OUTER_BOUND('',#822,.T.) ;
#550=FACE_OUTER_BOUND('',#824,.T.) ;
#551=FACE_OUTER_BOUND('',#825,.T.) ;
#552=FACE_OUTER_BOUND('',#826,.T.) ;
#553=FACE_OUTER_BOUND('',#827,.T.) ;
#554=FACE_OUTER_BOUND('',#828,.T.) ;
#555=FACE_OUTER_BOUND('',#829,.T.) ;
#813=EDGE_LOOP('',(#3483,#3484,#3485,#3486)) ;
#814=EDGE_LOOP('',(#3487,#3488,#3489,#3490)) ;
#815=EDGE_LOOP('',(#3491,#3492,#3493,#3494)) ;
#816=EDGE_LOOP('',(#3495,#3496,#3497,#3498,#3499,#3500)) ;
#817=EDGE_LOOP('',(#3501,#3502,#3503,#3504)) ;
#818=EDGE_LOOP('',(#3505,#3506,#3507,#3508)) ;
#819=EDGE_LOOP('',(#3509,#3510,#3511,#3512)) ;
#820=EDGE_LOOP('',(#3513)) ;
#821=EDGE_LOOP('',(#3514,#3515,#3516,#3517,#3518,#3519)) ;
#822=EDGE_LOOP('',(#3520)) ;
#823=EDGE_LOOP('',(#3521)) ;
#824=EDGE_LOOP('',(#3522)) ;
#825=EDGE_LOOP('',(#3523,#3524,#3525,#3526)) ;
#826=EDGE_LOOP('',(#3527,#3528,#3529,#3530)) ;
#827=EDGE_LOOP('',(#3531,#3532,#3533,#3534)) ;
#828=EDGE_LOOP('',(#3535,#3536,#3537,#3538)) ;
#829=EDGE_LOOP('',(#3539,#3540,#3541,#3542)) ;
#1165=LINE('',#6620,#1525) ;
#1166=LINE('',#6622,#1526) ;
#1167=LINE('',#6624,#1527) ;
#1168=LINE('',#6625,#1528) ;
#1169=LINE('',#6629,#1529) ;
#1170=LINE('',#6630,#1530) ;
#1171=LINE('',#6631,#1531) ;
#1172=LINE('',#6634,#1532) ;
#1173=LINE('',#6636,#1533) ;
#1174=LINE('',#6637,#1534) ;
#1175=LINE('',#6640,#1535) ;
#1176=LINE('',#6642,#1536) ;
#1177=LINE('',#6643,#1537) ;
#1178=LINE('',#6646,#1538) ;
#1179=LINE('',#6647,#1539) ;
#1180=LINE('',#6650,#1540) ;
#1181=LINE('',#6651,#1541) ;
#1182=LINE('',#6653,#1542) ;
#1183=LINE('',#6670,#1543) ;
#1184=LINE('',#6677,#1544) ;
#1185=LINE('',#6680,#1545) ;
#1525=VECTOR('',#5481,1.) ;
#1526=VECTOR('',#5482,1.) ;
#1527=VECTOR('',#5483,1.) ;
#1528=VECTOR('',#5484,1.) ;
#1529=VECTOR('',#5487,1.) ;
#1530=VECTOR('',#5488,0.99999999999962) ;
#1531=VECTOR('',#5489,0.99999999999962) ;
#1532=VECTOR('',#5492,0.99999999999962) ;
#1533=VECTOR('',#5493,1.) ;
#1534=VECTOR('',#5494,0.99999999999962) ;
#1535=VECTOR('',#5497,0.99999999999962) ;
#1536=VECTOR('',#5498,1.) ;
#1537=VECTOR('',#5499,0.99999999999962) ;
#1538=VECTOR('',#5502,1.) ;
#1539=VECTOR('',#5503,0.99999999999962) ;
#1540=VECTOR('',#5506,0.99999999999962) ;
#1541=VECTOR('',#5507,1.) ;
#1542=VECTOR('',#5510,1.) ;
#1543=VECTOR('',#5533,5.) ;
#1544=VECTOR('',#5542,3.) ;
#1545=VECTOR('',#5547,2.5) ;
#1705=CIRCLE('',#4386,4.4) ;
#1706=CIRCLE('',#4388,5.) ;
#1707=CIRCLE('',#4389,3.25) ;
#1708=CIRCLE('',#4391,2.5) ;
#1709=CIRCLE('',#4393,0.6) ;
#1710=CIRCLE('',#4394,5.) ;
#1711=CIRCLE('',#4397,0.25) ;
#1712=CIRCLE('',#4398,3.) ;
#1713=CIRCLE('',#4400,3.) ;
#1993=VERTEX_POINT('',#6618) ;
#1994=VERTEX_POINT('',#6619) ;
#1995=VERTEX_POINT('',#6621) ;
#1996=VERTEX_POINT('',#6623) ;
#1997=VERTEX_POINT('',#6627) ;
#1998=VERTEX_POINT('',#6628) ;
#1999=VERTEX_POINT('',#6633) ;
#2000=VERTEX_POINT('',#6635) ;
#2001=VERTEX_POINT('',#6639) ;
#2002=VERTEX_POINT('',#6641) ;
#2003=VERTEX_POINT('',#6645) ;
#2004=VERTEX_POINT('',#6649) ;
#2005=VERTEX_POINT('',#6655) ;
#2006=VERTEX_POINT('',#6658) ;
#2007=VERTEX_POINT('',#6660) ;
#2008=VERTEX_POINT('',#6663) ;
#2009=VERTEX_POINT('',#6666) ;
#2010=VERTEX_POINT('',#6672) ;
#2011=VERTEX_POINT('',#6676) ;
#2495=EDGE_CURVE('',#1993,#1994,#1165,.T.) ;
#2496=EDGE_CURVE('',#1993,#1995,#1166,.T.) ;
#2497=EDGE_CURVE('',#1995,#1996,#1167,.T.) ;
#2498=EDGE_CURVE('',#1994,#1996,#1168,.T.) ;
#2499=EDGE_CURVE('',#1997,#1998,#1169,.T.) ;
#2500=EDGE_CURVE('',#1997,#1993,#1170,.T.) ;
#2501=EDGE_CURVE('',#1998,#1994,#1171,.T.) ;
#2502=EDGE_CURVE('',#1995,#1999,#1172,.T.) ;
#2503=EDGE_CURVE('',#1999,#2000,#1173,.T.) ;
#2504=EDGE_CURVE('',#1996,#2000,#1174,.T.) ;
#2505=EDGE_CURVE('',#2000,#2001,#1175,.T.) ;
#2506=EDGE_CURVE('',#2001,#2002,#1176,.T.) ;
#2507=EDGE_CURVE('',#2002,#1998,#1177,.T.) ;
#2508=EDGE_CURVE('',#2003,#2002,#1178,.T.) ;
#2509=EDGE_CURVE('',#2003,#1997,#1179,.T.) ;
#2510=EDGE_CURVE('',#1999,#2004,#1180,.T.) ;
#2511=EDGE_CURVE('',#2004,#2001,#1181,.T.) ;
#2512=EDGE_CURVE('',#2004,#2003,#1182,.T.) ;
#2513=EDGE_CURVE('',#2005,#2005,#1705,.T.) ;
#2514=EDGE_CURVE('',#2006,#2006,#1706,.T.) ;
#2515=EDGE_CURVE('',#2007,#2007,#1707,.T.) ;
#2516=EDGE_CURVE('',#2008,#2008,#1708,.T.) ;
#2517=EDGE_CURVE('',#2005,#2009,#1709,.T.) ;
#2518=EDGE_CURVE('',#2009,#2009,#1710,.T.) ;
#2519=EDGE_CURVE('',#2009,#2006,#1183,.T.) ;
#2520=EDGE_CURVE('',#2007,#2010,#1711,.T.) ;
#2521=EDGE_CURVE('',#2010,#2010,#1712,.T.) ;
#2522=EDGE_CURVE('',#2010,#2011,#1184,.T.) ;
#2523=EDGE_CURVE('',#2011,#2011,#1713,.T.) ;
#2524=EDGE_CURVE('',#2011,#2008,#1185,.T.) ;
#3483=ORIENTED_EDGE('',*,*,#2495,.F.) ;
#3484=ORIENTED_EDGE('',*,*,#2496,.T.) ;
#3485=ORIENTED_EDGE('',*,*,#2497,.T.) ;
#3486=ORIENTED_EDGE('',*,*,#2498,.F.) ;
#3487=ORIENTED_EDGE('',*,*,#2499,.F.) ;
#3488=ORIENTED_EDGE('',*,*,#2500,.T.) ;
#3489=ORIENTED_EDGE('',*,*,#2495,.T.) ;
#3490=ORIENTED_EDGE('',*,*,#2501,.F.) ;
#3491=ORIENTED_EDGE('',*,*,#2497,.F.) ;
#3492=ORIENTED_EDGE('',*,*,#2502,.T.) ;
#3493=ORIENTED_EDGE('',*,*,#2503,.T.) ;
#3494=ORIENTED_EDGE('',*,*,#2504,.F.) ;
#3495=ORIENTED_EDGE('',*,*,#2498,.T.) ;
#3496=ORIENTED_EDGE('',*,*,#2504,.T.) ;
#3497=ORIENTED_EDGE('',*,*,#2505,.T.) ;
#3498=ORIENTED_EDGE('',*,*,#2506,.T.) ;
#3499=ORIENTED_EDGE('',*,*,#2507,.T.) ;
#3500=ORIENTED_EDGE('',*,*,#2501,.T.) ;
#3501=ORIENTED_EDGE('',*,*,#2508,.F.) ;
#3502=ORIENTED_EDGE('',*,*,#2509,.T.) ;
#3503=ORIENTED_EDGE('',*,*,#2499,.T.) ;
#3504=ORIENTED_EDGE('',*,*,#2507,.F.) ;
#3505=ORIENTED_EDGE('',*,*,#2503,.F.) ;
#3506=ORIENTED_EDGE('',*,*,#2510,.T.) ;
#3507=ORIENTED_EDGE('',*,*,#2511,.T.) ;
#3508=ORIENTED_EDGE('',*,*,#2505,.F.) ;
#3509=ORIENTED_EDGE('',*,*,#2511,.F.) ;
#3510=ORIENTED_EDGE('',*,*,#2512,.T.) ;
#3511=ORIENTED_EDGE('',*,*,#2508,.T.) ;
#3512=ORIENTED_EDGE('',*,*,#2506,.F.) ;
#3513=ORIENTED_EDGE('',*,*,#2513,.T.) ;
#3514=ORIENTED_EDGE('',*,*,#2509,.F.) ;
#3515=ORIENTED_EDGE('',*,*,#2512,.F.) ;
#3516=ORIENTED_EDGE('',*,*,#2510,.F.) ;
#3517=ORIENTED_EDGE('',*,*,#2502,.F.) ;
#3518=ORIENTED_EDGE('',*,*,#2496,.F.) ;
#3519=ORIENTED_EDGE('',*,*,#2500,.F.) ;
#3520=ORIENTED_EDGE('',*,*,#2514,.F.) ;
#3521=ORIENTED_EDGE('',*,*,#2515,.T.) ;
#3522=ORIENTED_EDGE('',*,*,#2516,.F.) ;
#3523=ORIENTED_EDGE('',*,*,#2513,.F.) ;
#3524=ORIENTED_EDGE('',*,*,#2517,.T.) ;
#3525=ORIENTED_EDGE('',*,*,#2518,.T.) ;
#3526=ORIENTED_EDGE('',*,*,#2517,.F.) ;
#3527=ORIENTED_EDGE('',*,*,#2518,.F.) ;
#3528=ORIENTED_EDGE('',*,*,#2519,.T.) ;
#3529=ORIENTED_EDGE('',*,*,#2514,.T.) ;
#3530=ORIENTED_EDGE('',*,*,#2519,.F.) ;
#3531=ORIENTED_EDGE('',*,*,#2515,.F.) ;
#3532=ORIENTED_EDGE('',*,*,#2520,.T.) ;
#3533=ORIENTED_EDGE('',*,*,#2521,.T.) ;
#3534=ORIENTED_EDGE('',*,*,#2520,.F.) ;
#3535=ORIENTED_EDGE('',*,*,#2521,.F.) ;
#3536=ORIENTED_EDGE('',*,*,#2522,.T.) ;
#3537=ORIENTED_EDGE('',*,*,#2523,.T.) ;
#3538=ORIENTED_EDGE('',*,*,#2522,.F.) ;
#3539=ORIENTED_EDGE('',*,*,#2523,.F.) ;
#3540=ORIENTED_EDGE('',*,*,#2524,.T.) ;
#3541=ORIENTED_EDGE('',*,*,#2516,.T.) ;
#3542=ORIENTED_EDGE('',*,*,#2524,.F.) ;
#3647=CYLINDRICAL_SURFACE('',#4395,5.) ;
#3648=CYLINDRICAL_SURFACE('',#4399,3.) ;
#3865=ADVANCED_FACE('',(#541),#243,.T.) ;
#3866=ADVANCED_FACE('',(#542),#244,.T.) ;
#3867=ADVANCED_FACE('',(#543),#245,.T.) ;
#3868=ADVANCED_FACE('',(#544),#246,.T.) ;
#3869=ADVANCED_FACE('',(#545),#247,.T.) ;
#3870=ADVANCED_FACE('',(#546),#248,.T.) ;
#3871=ADVANCED_FACE('',(#547),#249,.T.) ;
#3872=ADVANCED_FACE('',(#548,#131),#250,.T.) ;
#3873=ADVANCED_FACE('',(#549,#132),#251,.F.) ;
#3874=ADVANCED_FACE('',(#550),#252,.F.) ;
#3875=ADVANCED_FACE('',(#551),#55,.T.) ;
#3876=ADVANCED_FACE('',(#552),#3647,.T.) ;
#3877=ADVANCED_FACE('',(#553),#56,.F.) ;
#3878=ADVANCED_FACE('',(#554),#3648,.T.) ;
#3879=ADVANCED_FACE('',(#555),#325,.T.) ;
#3903=CLOSED_SHELL('',(#3865,#3866,#3867,#3868,#3869,#3870,#3871,#3872,
#3873,#3874,#3875,#3876,#3877,#3878,#3879)) ;
#4377=AXIS2_PLACEMENT_3D('',#6616,#5477,#5478) ;
#4378=AXIS2_PLACEMENT_3D('',#6617,#5479,#5480) ;
#4379=AXIS2_PLACEMENT_3D('',#6626,#5485,#5486) ;
#4380=AXIS2_PLACEMENT_3D('',#6632,#5490,#5491) ;
#4381=AXIS2_PLACEMENT_3D('',#6638,#5495,#5496) ;
#4382=AXIS2_PLACEMENT_3D('',#6644,#5500,#5501) ;
#4383=AXIS2_PLACEMENT_3D('',#6648,#5504,#5505) ;
#4384=AXIS2_PLACEMENT_3D('',#6652,#5508,#5509) ;
#4385=AXIS2_PLACEMENT_3D('',#6654,#5511,#5512) ;
#4386=AXIS2_PLACEMENT_3D('',#6656,#5513,#5514) ;
#4387=AXIS2_PLACEMENT_3D('',#6657,#5515,#5516) ;
#4388=AXIS2_PLACEMENT_3D('',#6659,#5517,#5518) ;
#4389=AXIS2_PLACEMENT_3D('',#6661,#5519,#5520) ;
#4390=AXIS2_PLACEMENT_3D('',#6662,#5521,#5522) ;
#4391=AXIS2_PLACEMENT_3D('',#6664,#5523,#5524) ;
#4392=AXIS2_PLACEMENT_3D('',#6665,#5525,#5526) ;
#4393=AXIS2_PLACEMENT_3D('',#6667,#5527,#5528) ;
#4394=AXIS2_PLACEMENT_3D('',#6668,#5529,#5530) ;
#4395=AXIS2_PLACEMENT_3D('',#6669,#5531,#5532) ;
#4396=AXIS2_PLACEMENT_3D('',#6671,#5534,#5535) ;
#4397=AXIS2_PLACEMENT_3D('',#6673,#5536,#5537) ;
#4398=AXIS2_PLACEMENT_3D('',#6674,#5538,#5539) ;
#4399=AXIS2_PLACEMENT_3D('',#6675,#5540,#5541) ;
#4400=AXIS2_PLACEMENT_3D('',#6678,#5543,#5544) ;
#4401=AXIS2_PLACEMENT_3D('',#6679,#5545,#5546) ;
#5477=DIRECTION('axis',(0.,0.,1.)) ;
#5478=DIRECTION('refdir',(1.,0.,0.)) ;
#5479=DIRECTION('center_axis',(1.,0.,-1.53837014911E-16)) ;
#5480=DIRECTION('ref_axis',(-1.53837014911E-16,0.,-1.)) ;
#5481=DIRECTION('',(0.,1.,0.)) ;
#5482=DIRECTION('',(0.,0.,-1.)) ;
#5483=DIRECTION('',(0.,1.,0.)) ;
#5484=DIRECTION('',(0.,0.,-1.)) ;
#5485=DIRECTION('center_axis',(0.50000000000019,0.,-0.866025403784329)) ;
#5486=DIRECTION('ref_axis',(-0.866025403784329,0.,-0.50000000000019)) ;
#5487=DIRECTION('',(0.,1.,0.)) ;
#5488=DIRECTION('',(-0.866025403784329,0.,-0.50000000000019)) ;
#5489=DIRECTION('',(-0.866025403784329,0.,-0.50000000000019)) ;
#5490=DIRECTION('center_axis',(0.50000000000019,0.,0.866025403784329)) ;
#5491=DIRECTION('ref_axis',(0.866025403784329,0.,-0.50000000000019)) ;
#5492=DIRECTION('',(0.866025403784329,0.,-0.50000000000019)) ;
#5493=DIRECTION('',(0.,1.,0.)) ;
#5494=DIRECTION('',(0.866025403784329,0.,-0.50000000000019)) ;
#5495=DIRECTION('center_axis',(0.,-1.,0.)) ;
#5496=DIRECTION('ref_axis',(1.,0.,0.)) ;
#5497=DIRECTION('',(0.866025403784329,0.,0.50000000000019)) ;
#5498=DIRECTION('',(0.,0.,1.)) ;
#5499=DIRECTION('',(-0.866025403784329,0.,0.50000000000019)) ;
#5500=DIRECTION('center_axis',(-0.50000000000019,0.,-0.866025403784329)) ;
#5501=DIRECTION('ref_axis',(-0.866025403784329,0.,0.50000000000019)) ;
#5502=DIRECTION('',(0.,1.,0.)) ;
#5503=DIRECTION('',(-0.866025403784329,0.,0.50000000000019)) ;
#5504=DIRECTION('center_axis',(-0.50000000000019,0.,0.866025403784329)) ;
#5505=DIRECTION('ref_axis',(0.866025403784329,0.,0.50000000000019)) ;
#5506=DIRECTION('',(0.866025403784329,0.,0.50000000000019)) ;
#5507=DIRECTION('',(0.,1.,0.)) ;
#5508=DIRECTION('center_axis',(-1.,0.,0.)) ;
#5509=DIRECTION('ref_axis',(0.,0.,1.)) ;
#5510=DIRECTION('',(0.,0.,1.)) ;
#5511=DIRECTION('center_axis',(0.,-1.,0.)) ;
#5512=DIRECTION('ref_axis',(-1.,0.,0.)) ;
#5513=DIRECTION('center_axis',(0.,-1.,0.)) ;
#5514=DIRECTION('ref_axis',(0.,0.,1.)) ;
#5515=DIRECTION('center_axis',(0.,-1.,0.)) ;
#5516=DIRECTION('ref_axis',(-1.,0.,0.)) ;
#5517=DIRECTION('center_axis',(0.,-1.,0.)) ;
#5518=DIRECTION('ref_axis',(0.,0.,1.)) ;
#5519=DIRECTION('center_axis',(0.,-1.,0.)) ;
#5520=DIRECTION('ref_axis',(0.,0.,1.)) ;
#5521=DIRECTION('center_axis',(0.,-1.,0.)) ;
#5522=DIRECTION('ref_axis',(-1.,0.,0.)) ;
#5523=DIRECTION('center_axis',(0.,-1.,0.)) ;
#5524=DIRECTION('ref_axis',(0.,0.,1.)) ;
#5525=DIRECTION('center_axis',(0.,-1.,0.)) ;
#5526=DIRECTION('ref_axis',(0.479425538604205,0.,-0.877582561890372)) ;
#5527=DIRECTION('center_axis',(-0.877582561890372,0.,-0.479425538604205)) ;
#5528=DIRECTION('ref_axis',(-0.479425538604205,0.,0.877582561890372)) ;
#5529=DIRECTION('center_axis',(0.,-1.,0.)) ;
#5530=DIRECTION('ref_axis',(0.,0.,1.)) ;
#5531=DIRECTION('center_axis',(0.,-1.,0.)) ;
#5532=DIRECTION('ref_axis',(0.479425538604204,0.,-0.877582561890372)) ;
#5533=DIRECTION('',(0.,1.,0.)) ;
#5534=DIRECTION('center_axis',(0.,-1.,0.)) ;
#5535=DIRECTION('ref_axis',(0.479425538604204,0.,-0.877582561890372)) ;
#5536=DIRECTION('center_axis',(0.877582561890372,0.,0.479425538604204)) ;
#5537=DIRECTION('ref_axis',(-0.479425538604204,0.,0.877582561890372)) ;
#5538=DIRECTION('center_axis',(0.,-1.,0.)) ;
#5539=DIRECTION('ref_axis',(0.,0.,1.)) ;
#5540=DIRECTION('center_axis',(0.,-1.,0.)) ;
#5541=DIRECTION('ref_axis',(0.479425538604204,0.,-0.877582561890372)) ;
#5542=DIRECTION('',(0.,1.,0.)) ;
#5543=DIRECTION('center_axis',(0.,-1.,0.)) ;
#5544=DIRECTION('ref_axis',(0.,0.,1.)) ;
#5545=DIRECTION('center_axis',(0.,-1.,0.)) ;
#5546=DIRECTION('ref_axis',(0.479425538604204,0.,-0.877582561890372)) ;
#5547=DIRECTION('',(0.339005049420894,0.707106781186865,-0.620544580563467)) ;
#6616=CARTESIAN_POINT('',(0.,0.,0.)) ;
#6617=CARTESIAN_POINT('Origin',(32.5,-26.,11.443375673)) ;
#6618=CARTESIAN_POINT('',(32.5,-26.,11.443375673)) ;
#6619=CARTESIAN_POINT('',(32.5,-23.,11.443375673)) ;
#6620=CARTESIAN_POINT('',(32.5,-24.5,11.443375673)) ;
#6621=CARTESIAN_POINT('',(32.5,-26.,8.55662432703)) ;
#6622=CARTESIAN_POINT('',(32.5,-26.,10.)) ;
#6623=CARTESIAN_POINT('',(32.5,-23.,8.55662432703)) ;
#6624=CARTESIAN_POINT('',(32.5,-24.5,8.55662432703)) ;
#6625=CARTESIAN_POINT('',(32.5,-23.,10.)) ;
#6626=CARTESIAN_POINT('Origin',(35.,-26.,12.8867513459)) ;
#6627=CARTESIAN_POINT('',(35.,-26.,12.8867513459)) ;
#6628=CARTESIAN_POINT('',(35.,-23.,12.8867513459)) ;
#6629=CARTESIAN_POINT('',(35.,-24.5,12.8867513459)) ;
#6630=CARTESIAN_POINT('',(33.75,-26.,12.1650635095)) ;
#6631=CARTESIAN_POINT('',(33.75,-23.,12.1650635095)) ;
#6632=CARTESIAN_POINT('Origin',(32.5,-26.,8.55662432703)) ;
#6633=CARTESIAN_POINT('',(35.,-26.,7.11324865405)) ;
#6634=CARTESIAN_POINT('',(33.75,-26.,7.83493649054)) ;
#6635=CARTESIAN_POINT('',(35.,-23.,7.11324865405)) ;
#6636=CARTESIAN_POINT('',(35.,-24.5,7.11324865405)) ;
#6637=CARTESIAN_POINT('',(33.75,-23.,7.83493649054)) ;
#6638=CARTESIAN_POINT('Origin',(-35.,-23.,10.)) ;
#6639=CARTESIAN_POINT('',(37.5,-23.,8.55662432703)) ;
#6640=CARTESIAN_POINT('',(36.25,-23.,7.83493649054)) ;
#6641=CARTESIAN_POINT('',(37.5,-23.,11.443375673)) ;
#6642=CARTESIAN_POINT('',(37.5,-23.,10.)) ;
#6643=CARTESIAN_POINT('',(36.25,-23.,12.1650635095)) ;
#6644=CARTESIAN_POINT('Origin',(37.5,-26.,11.443375673)) ;
#6645=CARTESIAN_POINT('',(37.5,-26.,11.443375673)) ;
#6646=CARTESIAN_POINT('',(37.5,-24.5,11.443375673)) ;
#6647=CARTESIAN_POINT('',(36.25,-26.,12.1650635095)) ;
#6648=CARTESIAN_POINT('Origin',(35.,-26.,7.11324865405)) ;
#6649=CARTESIAN_POINT('',(37.5,-26.,8.55662432703)) ;
#6650=CARTESIAN_POINT('',(36.25,-26.,7.83493649054)) ;
#6651=CARTESIAN_POINT('',(37.5,-24.5,8.55662432703)) ;
#6652=CARTESIAN_POINT('Origin',(37.5,-26.,8.55662432703)) ;
#6653=CARTESIAN_POINT('',(37.5,-26.,10.)) ;
#6654=CARTESIAN_POINT('Origin',(-35.,-26.,10.)) ;
#6655=CARTESIAN_POINT('',(32.8905276301,-26.,13.8613632723)) ;
#6656=CARTESIAN_POINT('Origin',(35.,-26.,10.)) ;
#6657=CARTESIAN_POINT('Origin',(-35.,-20.,5.)) ;
#6658=CARTESIAN_POINT('',(32.602872307,-20.,14.3879128095)) ;
#6659=CARTESIAN_POINT('Origin',(35.,-20.,10.)) ;
#6660=CARTESIAN_POINT('',(33.4418669995,-20.,12.8521433261)) ;
#6661=CARTESIAN_POINT('Origin',(35.,-20.,10.)) ;
#6662=CARTESIAN_POINT('Origin',(-35.,40.,7.5)) ;
#6663=CARTESIAN_POINT('',(33.8014361535,40.,12.1939564047)) ;
#6664=CARTESIAN_POINT('Origin',(35.,40.,10.)) ;
#6665=CARTESIAN_POINT('Origin',(35.,-25.4,10.)) ;
#6666=CARTESIAN_POINT('',(32.602872307,-25.4,14.3879128095)) ;
#6667=CARTESIAN_POINT('Origin',(32.8905276301415,-25.4,13.8613632723176)) ;
#6668=CARTESIAN_POINT('Origin',(35.,-25.4,10.)) ;
#6669=CARTESIAN_POINT('Origin',(35.,7.,10.)) ;
#6670=CARTESIAN_POINT('',(32.602872306979,7.,14.3879128094519)) ;
#6671=CARTESIAN_POINT('Origin',(35.,-19.75,10.)) ;
#6672=CARTESIAN_POINT('',(33.5617233842,-19.75,12.6327476857)) ;
#6673=CARTESIAN_POINT('Origin',(33.4418669995363,-19.75,12.8521433261437)) ;
#6674=CARTESIAN_POINT('Origin',(35.,-19.75,10.)) ;
#6675=CARTESIAN_POINT('Origin',(35.,7.,10.)) ;
#6676=CARTESIAN_POINT('',(33.5617233842,39.5,12.6327476857)) ;
#6677=CARTESIAN_POINT('',(33.5617233841874,7.,12.6327476856711)) ;
#6678=CARTESIAN_POINT('Origin',(35.,39.5,10.)) ;
#6679=CARTESIAN_POINT('Origin',(35.,40.,10.)) ;
#6680=CARTESIAN_POINT('',(33.8014361534895,40.,12.1939564047259)) ;
#6765=UNCERTAINTY_MEASURE_WITH_UNIT(LENGTH_MEASURE(0.01),#6780,
'DISTANCE_ACCURACY_VALUE',
'Maximum model space distance between geometric entities at asserted c
onnectivities') ;
#6767=UNCERTAINTY_MEASURE_WITH_UNIT(LENGTH_MEASURE(0.01),#6780,
'DISTANCE_ACCURACY_VALUE',
'Maximum model space distance between geometric entities at asserted c
onnectivities') ;
#6777=(
GEOMETRIC_REPRESENTATION_CONTEXT(3)
GLOBAL_UNCERTAINTY_ASSIGNED_CONTEXT((#6765))
GLOBAL_UNIT_ASSIGNED_CONTEXT((#6780,#6782,#6783))
REPRESENTATION_CONTEXT('','3D')
) ;
#6779=(
GEOMETRIC_REPRESENTATION_CONTEXT(3)
GLOBAL_UNCERTAINTY_ASSIGNED_CONTEXT((#6767))
GLOBAL_UNIT_ASSIGNED_CONTEXT((#6780,#6782,#6783))
REPRESENTATION_CONTEXT('','3D')
) ;
#6780=(
LENGTH_UNIT()
NAMED_UNIT(*)
SI_UNIT(.MILLI.,.METRE.)
) ;
#6782=(
NAMED_UNIT(*)
PLANE_ANGLE_UNIT()
SI_UNIT($,.RADIAN.)
) ;
#6783=(
NAMED_UNIT(*)
SI_UNIT($,.STERADIAN.)
SOLID_ANGLE_UNIT()
) ;
#6793=SHAPE_DEFINITION_REPRESENTATION(#6804,#6825) ;
#6804=PRODUCT_DEFINITION_SHAPE('',$,#6837) ;
#6825=SHAPE_REPRESENTATION('',(#4377),#6777) ;
#6827=PRODUCT_DEFINITION_CONTEXT('part definition',#6862,'design') ;
#6837=PRODUCT_DEFINITION('Clamp_Bolt_3','Clamp_Bolt_3',#6848,#6827) ;
#6848=PRODUCT_DEFINITION_FORMATION('',$,#6873) ;
#6862=APPLICATION_CONTEXT(
'Core Data for Automotive Mechanical Design Process') ;
#6863=PRODUCT_CONTEXT('part definition',#6862,'mechanical') ;
#6873=PRODUCT('Clamp_Bolt_3','Clamp_Bolt_3',$,(#6863)) ;
#6877=PRESENTATION_STYLE_ASSIGNMENT((#6880)) ;
#6880=SURFACE_STYLE_USAGE(.BOTH.,#6883) ;
#6883=SURFACE_SIDE_STYLE('',(#6886)) ;
#6886=SURFACE_STYLE_FILL_AREA(#6889) ;
#6889=FILL_AREA_STYLE('Opaque(203,203,203)',(#6892)) ;
#6892=FILL_AREA_STYLE_COLOUR('Opaque(203,203,203)',#6895) ;
#6895=COLOUR_RGB('Opaque(203,203,203)', 0.31764706, 0.68627451, 0.89019608) ;
ENDSEC;
END-ISO-10303-21;
